ISO-10303-21;
HEADER;
FILE_DESCRIPTION (('STEP AP214'),
    '1' );
FILE_NAME ('circlip for shafts normal_din_Circlip DIN 471 - 10 x 1.step',
    '2026-10-27T08:02:39',
    ( '' ),
    ( '' ),
    'SwSTEP 2.0',
    'SolidWorks 2026',
    '' );
FILE_SCHEMA (( 'AUTOMOTIVE_DESIGN' ));
ENDSEC;

DATA;
#2=FACE_OUTER_BOUND ( 'NONE', #4897, .T. ) ;
#3=AXIS2_PLACEMENT_3D ( 'NONE', #7464, #2948, #5642 ) ;
#29=CYLINDRICAL_SURFACE ( 'NONE', #9817, 4.799999999999999822 ) ;
#35=ADVANCED_FACE ( 'NONE', ( #6155 ), #7977, .T. ) ;
#38=EDGE_CURVE ( 'NONE', #10710, #279, #12151, .T. ) ;
#45=DIRECTION ( 'NONE',  ( 0.03086419753086420623, -0.9995235871707959241, 0.000000000000000000 ) ) ;
#91=CARTESIAN_POINT ( 'NONE',  ( 3.098410542199072637, -7.060458129626440815, -1.000000000000000000 ) ) ;
#127=EDGE_CURVE ( 'NONE', #10133, #6749, #9113, .T. ) ;
#132=PRODUCT ( 'circlip for shafts normal_din_Circlip DIN 471 - 10 x 1', 'circlip for shafts normal_din_Circlip DIN 471 - 10 x 1', '', ( #2666 ) ) ;
#150=DIRECTION ( 'NONE',  ( 1.000000000000000000, 0.000000000000000000, 0.000000000000000000 ) ) ;
#160=FACE_OUTER_BOUND ( 'NONE', #3496, .T. ) ;
#176=ORIENTED_EDGE ( 'NONE', *, *, #434, .T. ) ;
#187=VECTOR ( 'NONE', #9799, 999.9999999999998863 ) ;
#204=ORIENTED_EDGE ( 'NONE', *, *, #38, .F. ) ;
#211=ORIENTED_EDGE ( 'NONE', *, *, #8369, .F. ) ;
#212=CARTESIAN_POINT ( 'NONE',  ( 0.000000000000000000, 0.000000000000000000, 0.000000000000000000 ) ) ;
#215=FACE_OUTER_BOUND ( 'NONE', #11653, .T. ) ;
#242=VECTOR ( 'NONE', #2897, 1000.000000000000000 ) ;
#244=ORIENTED_EDGE ( 'NONE', *, *, #2101, .F. ) ;
#267=VECTOR ( 'NONE', #3186, 1000.000000000000114 ) ;
#276=DIRECTION ( 'NONE',  ( 0.000000000000000000, 0.000000000000000000, 1.000000000000000000 ) ) ;
#279=VERTEX_POINT ( 'NONE', #954 ) ;
#282=FACE_BOUND ( 'NONE', #6825, .T. ) ;
#283=EDGE_CURVE ( 'NONE', #6930, #9343, #6993, .T. ) ;
#290=CARTESIAN_POINT ( 'NONE',  ( -1.250000000000000000, -6.429618962271402616, -1.000000000000000000 ) ) ;
#307=FACE_OUTER_BOUND ( 'NONE', #11547, .T. ) ;
#331=VERTEX_POINT ( 'NONE', #8192 ) ;
#337=DIRECTION ( 'NONE',  ( 0.000000000000000000, 0.000000000000000000, 1.000000000000000000 ) ) ;
#372=CARTESIAN_POINT ( 'NONE',  ( -2.000000000000000000, -6.429618962271402616, 0.000000000000000000 ) ) ;
#379=CARTESIAN_POINT ( 'NONE',  ( 6.080745460913608902, 0.5192545390863916310, -1.000000000000000000 ) ) ;
#395=AXIS2_PLACEMENT_3D ( 'NONE', #290, #10783, #1338 ) ;
#399=PLANE ( 'NONE',  #10583 ) ;
#412=ADVANCED_FACE ( 'NONE', ( #1443 ), #5260, .T. ) ;
#423=ORIENTED_EDGE ( 'NONE', *, *, #10700, .T. ) ;
#431=ADVANCED_FACE ( 'NONE', ( #738 ), #686, .F. ) ;
#434=EDGE_CURVE ( 'NONE', #4082, #4193, #4789, .T. ) ;
#445=ORIENTED_EDGE ( 'NONE', *, *, #2739, .T. ) ;
#467=EDGE_LOOP ( 'NONE', ( #2592, #10546 ) ) ;
#470=DIRECTION ( 'NONE',  ( 0.03086419753086420623, -0.9995235871707959241, 0.000000000000000000 ) ) ;
#477=VERTEX_POINT ( 'NONE', #2804 ) ;
#485=EDGE_CURVE ( 'NONE', #331, #5149, #6388, .T. ) ;
#545=ORIENTED_EDGE ( 'NONE', *, *, #3935, .T. ) ;
#559=FACE_OUTER_BOUND ( 'NONE', #11903, .T. ) ;
#569=CARTESIAN_POINT ( 'NONE',  ( 2.595115354961440524, -7.673029147243177306, 0.000000000000000000 ) ) ;
#583=DIRECTION ( 'NONE',  ( 1.000000000000000000, 0.000000000000000000, 0.000000000000000000 ) ) ;
#601=DIRECTION ( 'NONE',  ( -1.000000000000000000, 0.000000000000000000, 0.000000000000000000 ) ) ;
#658=EDGE_CURVE ( 'NONE', #4082, #4830, #4877, .T. ) ;
#686=CYLINDRICAL_SURFACE ( 'NONE', #10173, 0.7500000000000000000 ) ;
#701=CYLINDRICAL_SURFACE ( 'NONE', #1923, 2.396904916527700102 ) ;
#738=FACE_OUTER_BOUND ( 'NONE', #6740, .T. ) ;
#744=LINE ( 'NONE', #7334, #3036 ) ;
#765=CARTESIAN_POINT ( 'NONE',  ( 3.309651814758565180, -5.455921364805393026, 0.000000000000000000 ) ) ;
#808=AXIS2_PLACEMENT_3D ( 'NONE', #8681, #7740, #7549 ) ;
#851=CARTESIAN_POINT ( 'NONE',  ( -0.1481481481481481122, -4.797713218419819903, -1.000000000000000000 ) ) ;
#860=EDGE_LOOP ( 'NONE', ( #11769, #4561 ) ) ;
#864=FILL_AREA_STYLE_COLOUR ( '', #1845 ) ;
#889=CARTESIAN_POINT ( 'NONE',  ( -5.686050877451574337, -5.768780236673276995, -1.000000000000000000 ) ) ;
#907=ORIENTED_EDGE ( 'NONE', *, *, #12203, .T. ) ;
#916=EDGE_CURVE ( 'NONE', #5149, #331, #3822, .T. ) ;
#919=CARTESIAN_POINT ( 'NONE',  ( 3.309651814758565180, -5.455921364805393026, -1.000000000000000000 ) ) ;
#934=ORIENTED_EDGE ( 'NONE', *, *, #8998, .T. ) ;
#939=EDGE_CURVE ( 'NONE', #1873, #5296, #2217, .T. ) ;
#941=CARTESIAN_POINT ( 'NONE',  ( 0.1481481481481481122, -4.797713218419819903, 0.000000000000000000 ) ) ;
#945=ORIENTED_EDGE ( 'NONE', *, *, #12203, .F. ) ;
#954=CARTESIAN_POINT ( 'NONE',  ( -2.000000000000000000, -6.429618962271402616, -1.000000000000000000 ) ) ;
#967=ORIENTED_EDGE ( 'NONE', *, *, #11197, .F. ) ;
#994=AXIS2_PLACEMENT_3D ( 'NONE', #5555, #4555, #9267 ) ;
#998=DIRECTION ( 'NONE',  ( -0.000000000000000000, -0.000000000000000000, -1.000000000000000000 ) ) ;
#1009=AXIS2_PLACEMENT_3D ( 'NONE', #919, #6687, #8735 ) ;
#1012=ORIENTED_EDGE ( 'NONE', *, *, #1063, .F. ) ;
#1021=AXIS2_PLACEMENT_3D ( 'NONE', #9496, #4732, #8552 ) ;
#1026=DIRECTION ( 'NONE',  ( -0.000000000000000000, -0.000000000000000000, -1.000000000000000000 ) ) ;
#1042=EDGE_CURVE ( 'NONE', #3494, #6198, #7409, .T. ) ;
#1045=DIRECTION ( 'NONE',  ( 0.000000000000000000, 0.000000000000000000, 1.000000000000000000 ) ) ;
#1063=EDGE_CURVE ( 'NONE', #6538, #7124, #2051, .T. ) ;
#1077=ADVANCED_FACE ( 'NONE', ( #3921 ), #10606, .T. ) ;
#1095=ORIENTED_EDGE ( 'NONE', *, *, #11677, .F. ) ;
#1102=EDGE_CURVE ( 'NONE', #10119, #2301, #6017, .T. ) ;
#1103=ORIENTED_EDGE ( 'NONE', *, *, #8592, .T. ) ;
#1140=ADVANCED_FACE ( 'NONE', ( #160 ), #7801, .T. ) ;
#1144=ORIENTED_EDGE ( 'NONE', *, *, #6176, .T. ) ;
#1146=DIRECTION ( 'NONE',  ( 1.000000000000000000, 0.000000000000000000, 0.000000000000000000 ) ) ;
#1150=EDGE_LOOP ( 'NONE', ( #1280, #8719, #3599, #5364 ) ) ;
#1179=DIRECTION ( 'NONE',  ( 0.000000000000000000, 0.000000000000000000, 1.000000000000000000 ) ) ;
#1201=DIRECTION ( 'NONE',  ( -0.000000000000000000, -0.000000000000000000, -1.000000000000000000 ) ) ;
#1202=ORIENTED_EDGE ( 'NONE', *, *, #2946, .F. ) ;
#1221=VECTOR ( 'NONE', #9353, 1000.000000000000000 ) ;
#1237=CIRCLE ( 'NONE', #4231, 2.396904916527700102 ) ;
#1243=ORIENTED_EDGE ( 'NONE', *, *, #6959, .F. ) ;
#1268=DIRECTION ( 'NONE',  ( 0.000000000000000000, 0.000000000000000000, 1.000000000000000000 ) ) ;
#1269=EDGE_CURVE ( 'NONE', #6377, #11243, #6158, .T. ) ;
#1280=ORIENTED_EDGE ( 'NONE', *, *, #939, .F. ) ;
#1292=ORIENTED_EDGE ( 'NONE', *, *, #11905, .T. ) ;
#1306=DIRECTION ( 'NONE',  ( 0.000000000000000000, 0.000000000000000000, 1.000000000000000000 ) ) ;
#1337=CARTESIAN_POINT ( 'NONE',  ( -3.309651814758565180, -5.455921364805393026, -1.000000000000000000 ) ) ;
#1338=DIRECTION ( 'NONE',  ( 1.000000000000000000, 0.000000000000000000, 0.000000000000000000 ) ) ;
#1394=FACE_BOUND ( 'NONE', #860, .T. ) ;
#1423=EDGE_CURVE ( 'NONE', #6198, #5296, #11216, .T. ) ;
#1440=MECHANICAL_DESIGN_GEOMETRIC_PRESENTATION_REPRESENTATION('',(#7846),#10219);
#1443=FACE_OUTER_BOUND ( 'NONE', #4634, .T. ) ;
#1501=DIRECTION ( 'NONE',  ( 1.000000000000000000, 0.000000000000000000, 0.000000000000000000 ) ) ;
#1517=ORIENTED_EDGE ( 'NONE', *, *, #6223, .T. ) ;
#1543=CARTESIAN_POINT ( 'NONE',  ( 1.250000000000000000, -6.429618962271402616, 0.000000000000000000 ) ) ;
#1548=( LENGTH_UNIT ( ) NAMED_UNIT ( * ) SI_UNIT ( .MILLI., .METRE. ) );
#1556=AXIS2_PLACEMENT_3D ( 'NONE', #9594, #1026, #6964 ) ;
#1572=EDGE_CURVE ( 'NONE', #3551, #4056, #8964, .T. ) ;
#1620=DIRECTION ( 'NONE',  ( 1.000000000000000000, 0.000000000000000000, 0.000000000000000000 ) ) ;
#1631=DIRECTION ( 'NONE',  ( 0.1305261922200524616, 0.9914448613738103822, -0.000000000000000000 ) ) ;
#1634=EDGE_CURVE ( 'NONE', #6930, #7756, #6913, .T. ) ;
#1650=CARTESIAN_POINT ( 'NONE',  ( -0.5000000000000000000, -6.429618962271402616, 0.000000000000000000 ) ) ;
#1662=LINE ( 'NONE', #765, #5799 ) ;
#1667=CARTESIAN_POINT ( 'NONE',  ( -1.250000000000000000, -6.429618962271402616, 0.000000000000000000 ) ) ;
#1688=DIRECTION ( 'NONE',  ( -0.000000000000000000, -0.000000000000000000, -1.000000000000000000 ) ) ;
#1717=DIRECTION ( 'NONE',  ( 1.000000000000000000, 0.000000000000000000, 0.000000000000000000 ) ) ;
#1753=ORIENTED_EDGE ( 'NONE', *, *, #5003, .F. ) ;
#1817=AXIS2_PLACEMENT_3D ( 'NONE', #2922, #2790, #1929 ) ;
#1818=CARTESIAN_POINT ( 'NONE',  ( 3.098410542199072637, -7.060458129626440815, 0.000000000000000000 ) ) ;
#1828=CYLINDRICAL_SURFACE ( 'NONE', #3, 6.080745460913608902 ) ;
#1845=COLOUR_RGB ( '',1.000000000000000000, 0.9490196078431372140, 0.9098039215686274384 ) ;
#1860=FACE_OUTER_BOUND ( 'NONE', #8206, .T. ) ;
#1873=VERTEX_POINT ( 'NONE', #569 ) ;
#1875=LINE ( 'NONE', #2799, #2102 ) ;
#1895=ADVANCED_FACE ( 'NONE', ( #9281 ), #701, .F. ) ;
#1903=CARTESIAN_POINT ( 'NONE',  ( 4.799999999999999822, 0.000000000000000000, 0.000000000000000000 ) ) ;
#1904=AXIS2_PLACEMENT_3D ( 'NONE', #5634, #7514, #8704 ) ;
#1906=EDGE_CURVE ( 'NONE', #9112, #5098, #8580, .T. ) ;
#1907=CARTESIAN_POINT ( 'NONE',  ( -2.354826896168714434, -6.962563485461402024, -1.000000000000000000 ) ) ;
#1908=ADVANCED_FACE ( 'NONE', ( #2 ), #1828, .T. ) ;
#1923=AXIS2_PLACEMENT_3D ( 'NONE', #889, #10569, #10383 ) ;
#1924=DIRECTION ( 'NONE',  ( 0.000000000000000000, 0.000000000000000000, 1.000000000000000000 ) ) ;
#1929=DIRECTION ( 'NONE',  ( 1.000000000000000000, 0.000000000000000000, 0.000000000000000000 ) ) ;
#1937=VERTEX_POINT ( 'NONE', #3758 ) ;
#1943=CARTESIAN_POINT ( 'NONE',  ( 0.1481481481481481122, -4.797713218419819903, -1.000000000000000000 ) ) ;
#1953=SHAPE_REPRESENTATION ( 'circlip for shafts normal_din_Circlip DIN 471 - 10 x 1', ( #6056 ), #3638 ) ;
#1973=ORIENTED_EDGE ( 'NONE', *, *, #1042, .F. ) ;
#1983=CARTESIAN_POINT ( 'NONE',  ( 0.000000000000000000, 0.5192545390863916310, -1.000000000000000000 ) ) ;
#1991=ADVANCED_FACE ( 'NONE', ( #12253 ), #2697, .T. ) ;
#1996=DIRECTION ( 'NONE',  ( 0.000000000000000000, 0.000000000000000000, 1.000000000000000000 ) ) ;
#2000=AXIS2_PLACEMENT_3D ( 'NONE', #4303, #2497, #1501 ) ;
#2024=CARTESIAN_POINT ( 'NONE',  ( -3.309651814758565180, -5.455921364805393026, 0.000000000000000000 ) ) ;
#2027=AXIS2_PLACEMENT_3D ( 'NONE', #9288, #9473, #6341 ) ;
#2028=AXIS2_PLACEMENT_3D ( 'NONE', #851, #7426, #5491 ) ;
#2037=EDGE_CURVE ( 'NONE', #4908, #7756, #8709, .T. ) ;
#2038=ORIENTED_EDGE ( 'NONE', *, *, #916, .T. ) ;
#2040=AXIS2_PLACEMENT_3D ( 'NONE', #7493, #1924, #5911 ) ;
#2051=LINE ( 'NONE', #5869, #7213 ) ;
#2054=ORIENTED_EDGE ( 'NONE', *, *, #11677, .T. ) ;
#2070=CARTESIAN_POINT ( 'NONE',  ( -0.1481481481481481122, -4.797713218419819903, 0.000000000000000000 ) ) ;
#2077=DIRECTION ( 'NONE',  ( 1.000000000000000000, 0.000000000000000000, 0.000000000000000000 ) ) ;
#2079=CARTESIAN_POINT ( 'NONE',  ( -3.309651814758565180, -5.455921364805393026, 0.000000000000000000 ) ) ;
#2101=EDGE_CURVE ( 'NONE', #3487, #7536, #3412, .T. ) ;
#2102=VECTOR ( 'NONE', #9558, 1000.000000000000000 ) ;
#2132=DIRECTION ( 'NONE',  ( 1.000000000000000000, 0.000000000000000000, 0.000000000000000000 ) ) ;
#2143=DIRECTION ( 'NONE',  ( 0.000000000000000000, 0.000000000000000000, 1.000000000000000000 ) ) ;
#2167=CARTESIAN_POINT ( 'NONE',  ( 0.2499999999999966416, -8.096141056083448362, 0.000000000000000000 ) ) ;
#2176=CYLINDRICAL_SURFACE ( 'NONE', #2869, 0.7500000000000000000 ) ;
#2214=PLANE ( 'NONE',  #9879 ) ;
#2217=CIRCLE ( 'NONE', #11790, 0.7499999999999997780 ) ;
#2218=DIRECTION ( 'NONE',  ( -0.9914448613738102711, -0.1305261922200524338, 0.000000000000000000 ) ) ;
#2237=DIRECTION ( 'NONE',  ( 1.000000000000000000, 0.000000000000000000, 0.000000000000000000 ) ) ;
#2245=ORIENTED_EDGE ( 'NONE', *, *, #1634, .T. ) ;
#2301=VERTEX_POINT ( 'NONE', #11599 ) ;
#2307=VECTOR ( 'NONE', #11500, 1000.000000000000000 ) ;
#2324=CARTESIAN_POINT ( 'NONE',  ( -3.098410542199071749, -7.060458129626440815, -1.000000000000000000 ) ) ;
#2332=CARTESIAN_POINT ( 'NONE',  ( 0.000000000000000000, 0.000000000000000000, -1.000000000000000000 ) ) ;
#2375=ORIENTED_EDGE ( 'NONE', *, *, #8013, .T. ) ;
#2424=FACE_OUTER_BOUND ( 'NONE', #7547, .T. ) ;
#2480=DIRECTION ( 'NONE',  ( 0.03086419753086420623, 0.9995235871707959241, -0.000000000000000000 ) ) ;
#2497=DIRECTION ( 'NONE',  ( 0.000000000000000000, 0.000000000000000000, 1.000000000000000000 ) ) ;
#2522=EDGE_LOOP ( 'NONE', ( #5996, #6162, #7863, #2245 ) ) ;
#2557=LINE ( 'NONE', #11254, #6438 ) ;
#2559=PLANE ( 'NONE',  #1904 ) ;
#2565=DIRECTION ( 'NONE',  ( 0.000000000000000000, 0.000000000000000000, 1.000000000000000000 ) ) ;
#2591=VECTOR ( 'NONE', #5529, 1000.000000000000000 ) ;
#2592=ORIENTED_EDGE ( 'NONE', *, *, #916, .F. ) ;
#2595=EDGE_LOOP ( 'NONE', ( #12212, #6420, #6566, #2038 ) ) ;
#2614=CARTESIAN_POINT ( 'NONE',  ( 0.000000000000000000, 0.000000000000000000, -1.000000000000000000 ) ) ;
#2617=CIRCLE ( 'NONE', #2027, 4.799999999999999822 ) ;
#2626=DIRECTION ( 'NONE',  ( 0.000000000000000000, 0.000000000000000000, 1.000000000000000000 ) ) ;
#2663=CARTESIAN_POINT ( 'NONE',  ( -4.078421086530219064, -3.990950201428956845, -1.000000000000000000 ) ) ;
#2666=PRODUCT_CONTEXT ( 'NONE', #11752, 'mechanical' ) ;
#2669=EDGE_LOOP ( 'NONE', ( #945, #244 ) ) ;
#2681=CIRCLE ( 'NONE', #10077, 2.396904916527699214 ) ;
#2691=DIRECTION ( 'NONE',  ( 1.000000000000000000, 0.000000000000000000, 0.000000000000000000 ) ) ;
#2696=CARTESIAN_POINT ( 'NONE',  ( -4.799999999999999822, 5.878304635907294211E-16, -1.000000000000000000 ) ) ;
#2697=CYLINDRICAL_SURFACE ( 'NONE', #4608, 8.099999999999999645 ) ;
#2738=DIRECTION ( 'NONE',  ( 0.000000000000000000, 0.000000000000000000, 1.000000000000000000 ) ) ;
#2739=EDGE_CURVE ( 'NONE', #10347, #4159, #4473, .T. ) ;
#2740=EDGE_CURVE ( 'NONE', #7756, #7721, #9229, .T. ) ;
#2781=DIRECTION ( 'NONE',  ( 0.000000000000000000, 0.000000000000000000, 1.000000000000000000 ) ) ;
#2790=DIRECTION ( 'NONE',  ( 0.000000000000000000, 0.000000000000000000, 1.000000000000000000 ) ) ;
#2797=SHAPE_REPRESENTATION_RELATIONSHIP ( 'NONE' , 'NONE' ,  #1953, #4814 ) ;
#2799=CARTESIAN_POINT ( 'NONE',  ( -0.5000000000000000000, -6.429618962271402616, -1.000000000000000000 ) ) ;
#2804=CARTESIAN_POINT ( 'NONE',  ( -4.078421086530219064, -3.990950201428956845, 0.000000000000000000 ) ) ;
#2825=VECTOR ( 'NONE', #2480, 1000.000000000000114 ) ;
#2832=CYLINDRICAL_SURFACE ( 'NONE', #8626, 4.799999999999999822 ) ;
#2849=EDGE_LOOP ( 'NONE', ( #6528, #7916, #3456, #10520 ) ) ;
#2869=AXIS2_PLACEMENT_3D ( 'NONE', #7941, #4121, #9754 ) ;
#2893=VECTOR ( 'NONE', #1268, 1000.000000000000000 ) ;
#2897=DIRECTION ( 'NONE',  ( 0.000000000000000000, 0.000000000000000000, 1.000000000000000000 ) ) ;
#2907=CYLINDRICAL_SURFACE ( 'NONE', #12173, 0.7500000000000000000 ) ;
#2911=LINE ( 'NONE', #4775, #10033 ) ;
#2922=CARTESIAN_POINT ( 'NONE',  ( 1.250000000000000000, -6.429618962271402616, -1.000000000000000000 ) ) ;
#2946=EDGE_CURVE ( 'NONE', #4193, #6538, #10897, .T. ) ;
#2948=DIRECTION ( 'NONE',  ( 0.000000000000000000, 0.000000000000000000, 1.000000000000000000 ) ) ;
#2949=CARTESIAN_POINT ( 'NONE',  ( 1.250000000000000000, -6.429618962271402616, -1.000000000000000000 ) ) ;
#2953=CARTESIAN_POINT ( 'NONE',  ( 0.000000000000000000, 0.000000000000000000, -1.000000000000000000 ) ) ;
#2965=FACE_OUTER_BOUND ( 'NONE', #10403, .T. ) ;
#3003=CIRCLE ( 'NONE', #395, 0.7500000000000000000 ) ;
#3036=VECTOR ( 'NONE', #3454, 1000.000000000000000 ) ;
#3040=CARTESIAN_POINT ( 'NONE',  ( 0.000000000000000000, 0.000000000000000000, -1.000000000000000000 ) ) ;
#3083=STYLED_ITEM('',(#12398),#4318);
#3115=LINE ( 'NONE', #6801, #187 ) ;
#3160=ORIENTED_EDGE ( 'NONE', *, *, #127, .T. ) ;
#3186=DIRECTION ( 'NONE',  ( 0.03086419753086420623, 0.9995235871707959241, -0.000000000000000000 ) ) ;
#3232=DIRECTION ( 'NONE',  ( 0.000000000000000000, 0.000000000000000000, 1.000000000000000000 ) ) ;
#3234=VECTOR ( 'NONE', #9728, 1000.000000000000000 ) ;
#3327=ORIENTED_EDGE ( 'NONE', *, *, #658, .F. ) ;
#3362=CARTESIAN_POINT ( 'NONE',  ( -0.5000000000000000000, -6.429618962271402616, -1.000000000000000000 ) ) ;
#3402=VECTOR ( 'NONE', #2781, 1000.000000000000000 ) ;
#3405=FACE_OUTER_BOUND ( 'NONE', #5536, .T. ) ;
#3412=CIRCLE ( 'NONE', #7005, 0.7500000000000000000 ) ;
#3441=AXIS2_PLACEMENT_3D ( 'NONE', #6123, #1306, #5120 ) ;
#3454=DIRECTION ( 'NONE',  ( 0.000000000000000000, 0.000000000000000000, 1.000000000000000000 ) ) ;
#3456=ORIENTED_EDGE ( 'NONE', *, *, #283, .T. ) ;
#3487=VERTEX_POINT ( 'NONE', #372 ) ;
#3494=VERTEX_POINT ( 'NONE', #4187 ) ;
#3496=EDGE_LOOP ( 'NONE', ( #4984, #1292, #3729, #1243 ) ) ;
#3497=DIRECTION ( 'NONE',  ( 0.000000000000000000, 0.000000000000000000, 1.000000000000000000 ) ) ;
#3551=VERTEX_POINT ( 'NONE', #12059 ) ;
#3553=( NAMED_UNIT ( * ) SI_UNIT ( $, .STERADIAN. ) SOLID_ANGLE_UNIT ( ) );
#3576=CARTESIAN_POINT ( 'NONE',  ( 6.080745460913608902, 0.5192545390863916310, -1.000000000000000000 ) ) ;
#3594=CARTESIAN_POINT ( 'NONE',  ( 0.5000000000000000000, -6.429618962271402616, -1.000000000000000000 ) ) ;
#3599=ORIENTED_EDGE ( 'NONE', *, *, #1042, .T. ) ;
#3638=( GEOMETRIC_REPRESENTATION_CONTEXT ( 3 ) GLOBAL_UNCERTAINTY_ASSIGNED_CONTEXT ( ( #8529 ) ) GLOBAL_UNIT_ASSIGNED_CONTEXT ( ( #1548, #4494, #3553 ) ) REPRESENTATION_CONTEXT ( 'NONE', 'WORKASPACE' ) );
#3695=DIRECTION ( 'NONE',  ( 1.000000000000000000, 0.000000000000000000, 0.000000000000000000 ) ) ;
#3702=APPLICATION_CONTEXT ( 'automotive_design' ) ;
#3705=CARTESIAN_POINT ( 'NONE',  ( -6.080745460913608902, 0.5192545390863924082, -1.000000000000000000 ) ) ;
#3729=ORIENTED_EDGE ( 'NONE', *, *, #12154, .T. ) ;
#3756=CARTESIAN_POINT ( 'NONE',  ( 5.686050877451574337, -5.768780236673276995, 0.000000000000000000 ) ) ;
#3758=CARTESIAN_POINT ( 'NONE',  ( -4.078421086530219064, -3.990950201428956845, -1.000000000000000000 ) ) ;
#3767=UNCERTAINTY_MEASURE_WITH_UNIT (LENGTH_MEASURE( 1.000000000000000082E-05 ), #4615, 'distance_accuracy_value', 'NONE');
#3769=ORIENTED_EDGE ( 'NONE', *, *, #1423, .F. ) ;
#3777=CARTESIAN_POINT ( 'NONE',  ( 0.000000000000000000, 0.000000000000000000, 0.000000000000000000 ) ) ;
#3781=DIRECTION ( 'NONE',  ( 1.000000000000000000, 0.000000000000000000, 0.000000000000000000 ) ) ;
#3822=CIRCLE ( 'NONE', #11185, 0.7500000000000000000 ) ;
#3874=SURFACE_SIDE_STYLE ('',( #11299 ) ) ;
#3880=ADVANCED_FACE ( 'NONE', ( #307 ), #2176, .F. ) ;
#3885=ORIENTED_EDGE ( 'NONE', *, *, #5870, .F. ) ;
#3903=ORIENTED_EDGE ( 'NONE', *, *, #5115, .F. ) ;
#3921=FACE_OUTER_BOUND ( 'NONE', #10251, .T. ) ;
#3930=ORIENTED_EDGE ( 'NONE', *, *, #4118, .F. ) ;
#3935=EDGE_CURVE ( 'NONE', #6749, #3551, #5063, .T. ) ;
#3991=DIRECTION ( 'NONE',  ( 0.000000000000000000, 0.000000000000000000, 1.000000000000000000 ) ) ;
#3992=AXIS2_PLACEMENT_3D ( 'NONE', #2614, #1688, #1620 ) ;
#4035=DIRECTION ( 'NONE',  ( 0.000000000000000000, 0.000000000000000000, 1.000000000000000000 ) ) ;
#4046=DIRECTION ( 'NONE',  ( 0.000000000000000000, 0.000000000000000000, 1.000000000000000000 ) ) ;
#4056=VERTEX_POINT ( 'NONE', #9202 ) ;
#4058=DIRECTION ( 'NONE',  ( 0.000000000000000000, 0.000000000000000000, 1.000000000000000000 ) ) ;
#4082=VERTEX_POINT ( 'NONE', #8096 ) ;
#4102=DIRECTION ( 'NONE',  ( 1.000000000000000000, 0.000000000000000000, 0.000000000000000000 ) ) ;
#4114=CARTESIAN_POINT ( 'NONE',  ( 2.000000000000000000, -6.429618962271402616, -1.000000000000000000 ) ) ;
#4118=EDGE_CURVE ( 'NONE', #4159, #6497, #5464, .T. ) ;
#4121=DIRECTION ( 'NONE',  ( 0.000000000000000000, 0.000000000000000000, 1.000000000000000000 ) ) ;
#4159=VERTEX_POINT ( 'NONE', #5695 ) ;
#4179=EDGE_CURVE ( 'NONE', #11838, #4672, #6680, .T. ) ;
#4187=CARTESIAN_POINT ( 'NONE',  ( 2.595115354961440524, -7.673029147243177306, -1.000000000000000000 ) ) ;
#4193=VERTEX_POINT ( 'NONE', #1943 ) ;
#4217=CARTESIAN_POINT ( 'NONE',  ( 0.1481481481481481122, -4.797713218419819903, -1.000000000000000000 ) ) ;
#4231=AXIS2_PLACEMENT_3D ( 'NONE', #4564, #7455, #2691 ) ;
#4280=CARTESIAN_POINT ( 'NONE',  ( 1.250000000000000000, -6.429618962271402616, -1.000000000000000000 ) ) ;
#4303=CARTESIAN_POINT ( 'NONE',  ( 0.000000000000000000, 0.000000000000000000, -1.000000000000000000 ) ) ;
#4304=ADVANCED_FACE ( 'NONE', ( #7822 ), #5065, .F. ) ;
#4315=CARTESIAN_POINT ( 'NONE',  ( -6.080745460913608902, 0.5192545390863924082, 0.000000000000000000 ) ) ;
#4318=MANIFOLD_SOLID_BREP ( 'Body', #10567 ) ;
#4323=CYLINDRICAL_SURFACE ( 'NONE', #7804, 0.7499999999999997780 ) ;
#4362=AXIS2_PLACEMENT_3D ( 'NONE', #12047, #6254, #4491 ) ;
#4364=LINE ( 'NONE', #11988, #8430 ) ;
#4374=CARTESIAN_POINT ( 'NONE',  ( 2.000000000000000000, -6.429618962271402616, 0.000000000000000000 ) ) ;
#4378=CARTESIAN_POINT ( 'NONE',  ( 3.309651814758564736, -5.455921364805393026, -1.000000000000000000 ) ) ;
#4410=ORIENTED_EDGE ( 'NONE', *, *, #434, .F. ) ;
#4431=AXIS2_PLACEMENT_3D ( 'NONE', #3756, #5826, #2077 ) ;
#4473=LINE ( 'NONE', #8296, #3234 ) ;
#4491=DIRECTION ( 'NONE',  ( 1.000000000000000000, 0.000000000000000000, 0.000000000000000000 ) ) ;
#4494=( NAMED_UNIT ( * ) PLANE_ANGLE_UNIT ( ) SI_UNIT ( $, .RADIAN. ) );
#4544=CYLINDRICAL_SURFACE ( 'NONE', #4577, 0.7499999999999997780 ) ;
#4547=( NAMED_UNIT ( * ) SI_UNIT ( $, .STERADIAN. ) SOLID_ANGLE_UNIT ( ) );
#4555=DIRECTION ( 'NONE',  ( 0.000000000000000000, 0.000000000000000000, 1.000000000000000000 ) ) ;
#4561=ORIENTED_EDGE ( 'NONE', *, *, #1102, .T. ) ;
#4564=CARTESIAN_POINT ( 'NONE',  ( -5.686050877451574337, -5.768780236673276995, -1.000000000000000000 ) ) ;
#4577=AXIS2_PLACEMENT_3D ( 'NONE', #11108, #3497, #7318 ) ;
#4589=DIRECTION ( 'NONE',  ( 0.1305261922200524616, 0.9914448613738103822, -0.000000000000000000 ) ) ;
#4591=DIRECTION ( 'NONE',  ( 0.000000000000000000, 0.000000000000000000, 1.000000000000000000 ) ) ;
#4596=AXIS2_PLACEMENT_3D ( 'NONE', #8211, #2565, #7285 ) ;
#4606=CARTESIAN_POINT ( 'NONE',  ( 2.354826896168714434, -6.962563485461402024, 0.000000000000000000 ) ) ;
#4608=AXIS2_PLACEMENT_3D ( 'NONE', #7714, #5571, #11315 ) ;
#4611=ADVANCED_FACE ( 'NONE', ( #282, #1394, #215 ), #2214, .F. ) ;
#4615=( LENGTH_UNIT ( ) NAMED_UNIT ( * ) SI_UNIT ( .MILLI., .METRE. ) );
#4634=EDGE_LOOP ( 'NONE', ( #8679, #8427, #1517, #3160 ) ) ;
#4649=LINE ( 'NONE', #8468, #242 ) ;
#4672=VERTEX_POINT ( 'NONE', #11089 ) ;
#4686=DIRECTION ( 'NONE',  ( 1.000000000000000000, 0.000000000000000000, 0.000000000000000000 ) ) ;
#4687=DIRECTION ( 'NONE',  ( 1.000000000000000000, 0.000000000000000000, 0.000000000000000000 ) ) ;
#4732=DIRECTION ( 'NONE',  ( 0.000000000000000000, 0.000000000000000000, 1.000000000000000000 ) ) ;
#4775=CARTESIAN_POINT ( 'NONE',  ( 0.1481481481481481122, -4.797713218419819903, -1.000000000000000000 ) ) ;
#4778=ORIENTED_EDGE ( 'NONE', *, *, #2037, .T. ) ;
#4780=DIRECTION ( 'NONE',  ( 0.000000000000000000, 0.000000000000000000, 1.000000000000000000 ) ) ;
#4789=CIRCLE ( 'NONE', #3992, 4.799999999999999822 ) ;
#4812=ORIENTED_EDGE ( 'NONE', *, *, #1269, .T. ) ;
#4814=ADVANCED_BREP_SHAPE_REPRESENTATION ( '', ( #4318, #6056 ), #3638 ) ;
#4825=VECTOR ( 'NONE', #4058, 1000.000000000000000 ) ;
#4828=CYLINDRICAL_SURFACE ( 'NONE', #7854, 0.7500000000000000000 ) ;
#4830=VERTEX_POINT ( 'NONE', #1903 ) ;
#4877=LINE ( 'NONE', #10437, #12166 ) ;
#4897=EDGE_LOOP ( 'NONE', ( #2375, #11782, #3930, #11070 ) ) ;
#4903=FACE_OUTER_BOUND ( 'NONE', #2595, .T. ) ;
#4908=VERTEX_POINT ( 'NONE', #2024 ) ;
#4918=CARTESIAN_POINT ( 'NONE',  ( -6.080745460913608902, 0.5192545390863924082, -1.000000000000000000 ) ) ;
#4957=EDGE_CURVE ( 'NONE', #6377, #10347, #2681, .T. ) ;
#4984=ORIENTED_EDGE ( 'NONE', *, *, #1906, .F. ) ;
#5003=EDGE_CURVE ( 'NONE', #8570, #6497, #6025, .T. ) ;
#5043=CARTESIAN_POINT ( 'NONE',  ( -1.250000000000000000, -6.429618962271402616, -1.000000000000000000 ) ) ;
#5058=DIRECTION ( 'NONE',  ( 0.000000000000000000, 0.000000000000000000, 1.000000000000000000 ) ) ;
#5062=CARTESIAN_POINT ( 'NONE',  ( -5.686050877451574337, -5.768780236673276995, 0.000000000000000000 ) ) ;
#5063=LINE ( 'NONE', #2070, #267 ) ;
#5065=CYLINDRICAL_SURFACE ( 'NONE', #8073, 4.799999999999999822 ) ;
#5098=VERTEX_POINT ( 'NONE', #4315 ) ;
#5115=EDGE_CURVE ( 'NONE', #4056, #4830, #5500, .T. ) ;
#5119=( NAMED_UNIT ( * ) PLANE_ANGLE_UNIT ( ) SI_UNIT ( $, .RADIAN. ) );
#5120=DIRECTION ( 'NONE',  ( 1.000000000000000000, 0.000000000000000000, 0.000000000000000000 ) ) ;
#5122=ORIENTED_EDGE ( 'NONE', *, *, #5661, .F. ) ;
#5149=VERTEX_POINT ( 'NONE', #4374 ) ;
#5152=CIRCLE ( 'NONE', #8969, 8.099999999999999645 ) ;
#5160=ORIENTED_EDGE ( 'NONE', *, *, #9838, .T. ) ;
#5173=ORIENTED_EDGE ( 'NONE', *, *, #4957, .F. ) ;
#5207=ORIENTED_EDGE ( 'NONE', *, *, #8592, .F. ) ;
#5231=ADVANCED_FACE ( 'NONE', ( #9146, #11129, #559 ), #2559, .T. ) ;
#5260=CYLINDRICAL_SURFACE ( 'NONE', #2000, 8.099999999999999645 ) ;
#5262=CARTESIAN_POINT ( 'NONE',  ( -0.2500000000000000000, -8.096141056083446585, -1.000000000000000000 ) ) ;
#5268=AXIS2_PLACEMENT_3D ( 'NONE', #7512, #998, #3695 ) ;
#5296=VERTEX_POINT ( 'NONE', #1818 ) ;
#5301=CARTESIAN_POINT ( 'NONE',  ( -0.1481481481481481122, -4.797713218419819903, -1.000000000000000000 ) ) ;
#5309=CYLINDRICAL_SURFACE ( 'NONE', #4362, 2.396904916527699214 ) ;
#5312=ORIENTED_EDGE ( 'NONE', *, *, #4118, .T. ) ;
#5313=CARTESIAN_POINT ( 'NONE',  ( -3.098410542199071749, -7.060458129626440815, -1.000000000000000000 ) ) ;
#5324=ORIENTED_EDGE ( 'NONE', *, *, #1572, .F. ) ;
#5327=ORIENTED_EDGE ( 'NONE', *, *, #11709, .T. ) ;
#5331=ORIENTED_EDGE ( 'NONE', *, *, #3935, .F. ) ;
#5364=ORIENTED_EDGE ( 'NONE', *, *, #1423, .T. ) ;
#5432=LINE ( 'NONE', #11976, #9778 ) ;
#5433=AXIS2_PLACEMENT_3D ( 'NONE', #3777, #4591, #1717 ) ;
#5434=ORIENTED_EDGE ( 'NONE', *, *, #1572, .T. ) ;
#5464=CIRCLE ( 'NONE', #10852, 6.080745460913608902 ) ;
#5491=DIRECTION ( 'NONE',  ( 0.03086419753086420623, 0.9995235871707959241, 0.000000000000000000 ) ) ;
#5500=CIRCLE ( 'NONE', #6899, 4.799999999999999822 ) ;
#5529=DIRECTION ( 'NONE',  ( 0.000000000000000000, 0.000000000000000000, 1.000000000000000000 ) ) ;
#5536=EDGE_LOOP ( 'NONE', ( #1012, #1202, #11825, #934 ) ) ;
#5555=CARTESIAN_POINT ( 'NONE',  ( 1.250000000000000000, -6.429618962271402616, 0.000000000000000000 ) ) ;
#5571=DIRECTION ( 'NONE',  ( 0.000000000000000000, 0.000000000000000000, 1.000000000000000000 ) ) ;
#5595=EDGE_LOOP ( 'NONE', ( #6751, #7590, #8283, #1753 ) ) ;
#5597=ORIENTED_EDGE ( 'NONE', *, *, #11905, .F. ) ;
#5603=DIRECTION ( 'NONE',  ( 0.000000000000000000, 0.000000000000000000, 1.000000000000000000 ) ) ;
#5634=CARTESIAN_POINT ( 'NONE',  ( 0.000000000000000000, 0.000000000000000000, 0.000000000000000000 ) ) ;
#5642=DIRECTION ( 'NONE',  ( 1.000000000000000000, 0.000000000000000000, 0.000000000000000000 ) ) ;
#5661=EDGE_CURVE ( 'NONE', #10710, #7536, #1875, .T. ) ;
#5677=DIRECTION ( 'NONE',  ( 0.000000000000000000, 0.000000000000000000, 1.000000000000000000 ) ) ;
#5695=CARTESIAN_POINT ( 'NONE',  ( 4.078421086530217288, -3.990950201428958621, 0.000000000000000000 ) ) ;
#5696=CARTESIAN_POINT ( 'NONE',  ( -0.1481481481481481122, -4.797713218419819903, -1.000000000000000000 ) ) ;
#5708=CARTESIAN_POINT ( 'NONE',  ( -3.098410542199071749, -7.060458129626440815, 0.000000000000000000 ) ) ;
#5721=DIRECTION ( 'NONE',  ( 1.000000000000000000, 0.000000000000000000, 0.000000000000000000 ) ) ;
#5738=ORIENTED_EDGE ( 'NONE', *, *, #939, .T. ) ;
#5799=VECTOR ( 'NONE', #4589, 999.9999999999998863 ) ;
#5826=DIRECTION ( 'NONE',  ( -0.000000000000000000, -0.000000000000000000, -1.000000000000000000 ) ) ;
#5869=CARTESIAN_POINT ( 'NONE',  ( 0.1481481481481481122, -4.797713218419819903, 0.000000000000000000 ) ) ;
#5870=EDGE_CURVE ( 'NONE', #2301, #5149, #10793, .T. ) ;
#5895=ORIENTED_EDGE ( 'NONE', *, *, #8013, .F. ) ;
#5911=DIRECTION ( 'NONE',  ( 1.000000000000000000, 0.000000000000000000, 0.000000000000000000 ) ) ;
#5972=DIRECTION ( 'NONE',  ( 1.000000000000000000, 0.000000000000000000, -0.000000000000000000 ) ) ;
#5991=CIRCLE ( 'NONE', #11560, 0.7500000000000000000 ) ;
#5996=ORIENTED_EDGE ( 'NONE', *, *, #2037, .F. ) ;
#6000=( LENGTH_UNIT ( ) NAMED_UNIT ( * ) SI_UNIT ( .MILLI., .METRE. ) );
#6016=EDGE_CURVE ( 'NONE', #10133, #11838, #11102, .T. ) ;
#6017=CIRCLE ( 'NONE', #1817, 0.7500000000000000000 ) ;
#6025=LINE ( 'NONE', #379, #2893 ) ;
#6034=CARTESIAN_POINT ( 'NONE',  ( 2.354826896168714434, -6.962563485461402024, -1.000000000000000000 ) ) ;
#6041=DIRECTION ( 'NONE',  ( 0.000000000000000000, 0.000000000000000000, 1.000000000000000000 ) ) ;
#6056=AXIS2_PLACEMENT_3D ( 'NONE', #212, #4035, #8864 ) ;
#6072=( GEOMETRIC_REPRESENTATION_CONTEXT ( 3 ) GLOBAL_UNCERTAINTY_ASSIGNED_CONTEXT ( ( #8407 ) ) GLOBAL_UNIT_ASSIGNED_CONTEXT ( ( #6000, #5119, #6892 ) ) REPRESENTATION_CONTEXT ( 'NONE', 'WORKASPACE' ) );
#6074=CARTESIAN_POINT ( 'NONE',  ( -0.2500000000000000000, -8.096141056083446585, 0.000000000000000000 ) ) ;
#6078=DIRECTION ( 'NONE',  ( 0.000000000000000000, 0.000000000000000000, 1.000000000000000000 ) ) ;
#6123=CARTESIAN_POINT ( 'NONE',  ( 0.000000000000000000, 0.5192545390863916310, -1.000000000000000000 ) ) ;
#6134=ORIENTED_EDGE ( 'NONE', *, *, #4179, .T. ) ;
#6147=CARTESIAN_POINT ( 'NONE',  ( 0.1481481481481481122, -4.797713218419819903, -1.000000000000000000 ) ) ;
#6152=ORIENTED_EDGE ( 'NONE', *, *, #6176, .F. ) ;
#6155=FACE_OUTER_BOUND ( 'NONE', #2522, .T. ) ;
#6158=LINE ( 'NONE', #11897, #11391 ) ;
#6162=ORIENTED_EDGE ( 'NONE', *, *, #10700, .F. ) ;
#6163=ADVANCED_FACE ( 'NONE', ( #1860 ), #11160, .T. ) ;
#6176=EDGE_CURVE ( 'NONE', #11838, #3551, #8355, .T. ) ;
#6198=VERTEX_POINT ( 'NONE', #8780 ) ;
#6200=LINE ( 'NONE', #9093, #7834 ) ;
#6207=VECTOR ( 'NONE', #10823, 999.9999999999998863 ) ;
#6223=EDGE_CURVE ( 'NONE', #9343, #10133, #8038, .T. ) ;
#6254=DIRECTION ( 'NONE',  ( 0.000000000000000000, 0.000000000000000000, 1.000000000000000000 ) ) ;
#6275=ORIENTED_EDGE ( 'NONE', *, *, #9919, .F. ) ;
#6292=DIRECTION ( 'NONE',  ( 1.000000000000000000, 0.000000000000000000, 0.000000000000000000 ) ) ;
#6307=ORIENTED_EDGE ( 'NONE', *, *, #11709, .F. ) ;
#6332=CARTESIAN_POINT ( 'NONE',  ( 6.080745460913608902, 0.5192545390863916310, 0.000000000000000000 ) ) ;
#6333=LINE ( 'NONE', #2696, #8804 ) ;
#6341=DIRECTION ( 'NONE',  ( 1.000000000000000000, 0.000000000000000000, 0.000000000000000000 ) ) ;
#6377=VERTEX_POINT ( 'NONE', #4378 ) ;
#6388=CIRCLE ( 'NONE', #994, 0.7500000000000000000 ) ;
#6420=ORIENTED_EDGE ( 'NONE', *, *, #8089, .F. ) ;
#6438=VECTOR ( 'NONE', #1631, 999.9999999999998863 ) ;
#6457=CARTESIAN_POINT ( 'NONE',  ( 0.000000000000000000, 0.000000000000000000, 0.000000000000000000 ) ) ;
#6497=VERTEX_POINT ( 'NONE', #6332 ) ;
#6519=EDGE_CURVE ( 'NONE', #11243, #4159, #9837, .T. ) ;
#6523=EDGE_LOOP ( 'NONE', ( #6134, #6948, #5324, #6152 ) ) ;
#6526=EDGE_LOOP ( 'NONE', ( #8488, #10036, #6934, #3885 ) ) ;
#6528=ORIENTED_EDGE ( 'NONE', *, *, #2740, .F. ) ;
#6530=CARTESIAN_POINT ( 'NONE',  ( 0.000000000000000000, 0.5192545390863916310, -1.000000000000000000 ) ) ;
#6538=VERTEX_POINT ( 'NONE', #941 ) ;
#6540=SHAPE_DEFINITION_REPRESENTATION ( #8724, #1953 ) ;
#6566=ORIENTED_EDGE ( 'NONE', *, *, #5870, .T. ) ;
#6593=FACE_OUTER_BOUND ( 'NONE', #5595, .T. ) ;
#6646=DIRECTION ( 'NONE',  ( 0.000000000000000000, 0.000000000000000000, 1.000000000000000000 ) ) ;
#6680=CIRCLE ( 'NONE', #5268, 4.799999999999999822 ) ;
#6687=DIRECTION ( 'NONE',  ( 0.9914448613738102711, -0.1305261922200524338, 0.000000000000000000 ) ) ;
#6731=DIRECTION ( 'NONE',  ( 0.03086419753086420623, -0.9995235871707959241, 0.000000000000000000 ) ) ;
#6740=EDGE_LOOP ( 'NONE', ( #6879, #7057, #8943, #5122 ) ) ;
#6749=VERTEX_POINT ( 'NONE', #6074 ) ;
#6751=ORIENTED_EDGE ( 'NONE', *, *, #9556, .T. ) ;
#6801=CARTESIAN_POINT ( 'NONE',  ( -3.309651814758565180, -5.455921364805393026, -1.000000000000000000 ) ) ;
#6825=EDGE_LOOP ( 'NONE', ( #9948, #8119 ) ) ;
#6879=ORIENTED_EDGE ( 'NONE', *, *, #8240, .F. ) ;
#6892=( NAMED_UNIT ( * ) SI_UNIT ( $, .STERADIAN. ) SOLID_ANGLE_UNIT ( ) );
#6899=AXIS2_PLACEMENT_3D ( 'NONE', #6457, #9276, #10940 ) ;
#6912=CARTESIAN_POINT ( 'NONE',  ( 1.250000000000000000, -6.429618962271402616, -1.000000000000000000 ) ) ;
#6913=LINE ( 'NONE', #2324, #10746 ) ;
#6930=VERTEX_POINT ( 'NONE', #5313 ) ;
#6934=ORIENTED_EDGE ( 'NONE', *, *, #485, .T. ) ;
#6948=ORIENTED_EDGE ( 'NONE', *, *, #8631, .T. ) ;
#6959=EDGE_CURVE ( 'NONE', #5098, #477, #10155, .T. ) ;
#6964=DIRECTION ( 'NONE',  ( 1.000000000000000000, 0.000000000000000000, 0.000000000000000000 ) ) ;
#6993=CIRCLE ( 'NONE', #8992, 0.7499999999999997780 ) ;
#7005=AXIS2_PLACEMENT_3D ( 'NONE', #9945, #6078, #2132 ) ;
#7016=CARTESIAN_POINT ( 'NONE',  ( 0.5000000000000000000, -6.429618962271402616, -1.000000000000000000 ) ) ;
#7057=ORIENTED_EDGE ( 'NONE', *, *, #9919, .T. ) ;
#7100=ORIENTED_EDGE ( 'NONE', *, *, #12154, .F. ) ;
#7124=VERTEX_POINT ( 'NONE', #2167 ) ;
#7142=VERTEX_POINT ( 'NONE', #11674 ) ;
#7144=EDGE_CURVE ( 'NONE', #10979, #3494, #5152, .T. ) ;
#7213=VECTOR ( 'NONE', #45, 1000.000000000000114 ) ;
#7249=AXIS2_PLACEMENT_3D ( 'NONE', #8400, #8334, #10264 ) ;
#7285=DIRECTION ( 'NONE',  ( 1.000000000000000000, 0.000000000000000000, 0.000000000000000000 ) ) ;
#7318=DIRECTION ( 'NONE',  ( 1.000000000000000000, 0.000000000000000000, 0.000000000000000000 ) ) ;
#7334=CARTESIAN_POINT ( 'NONE',  ( -2.595115354961444076, -7.673029147243174641, -1.000000000000000000 ) ) ;
#7409=CIRCLE ( 'NONE', #808, 0.7499999999999997780 ) ;
#7426=DIRECTION ( 'NONE',  ( 0.9995235871707960351, -0.03086419753086420970, 0.000000000000000000 ) ) ;
#7455=DIRECTION ( 'NONE',  ( -0.000000000000000000, -0.000000000000000000, -1.000000000000000000 ) ) ;
#7464=CARTESIAN_POINT ( 'NONE',  ( 0.000000000000000000, 0.5192545390863916310, -1.000000000000000000 ) ) ;
#7493=CARTESIAN_POINT ( 'NONE',  ( 0.000000000000000000, 0.000000000000000000, -1.000000000000000000 ) ) ;
#7512=CARTESIAN_POINT ( 'NONE',  ( 0.000000000000000000, 0.000000000000000000, -1.000000000000000000 ) ) ;
#7514=DIRECTION ( 'NONE',  ( 0.000000000000000000, 0.000000000000000000, 1.000000000000000000 ) ) ;
#7532=DIRECTION ( 'NONE',  ( 0.000000000000000000, 0.000000000000000000, 1.000000000000000000 ) ) ;
#7536=VERTEX_POINT ( 'NONE', #1650 ) ;
#7547=EDGE_LOOP ( 'NONE', ( #11667, #8371, #11372, #445 ) ) ;
#7549=DIRECTION ( 'NONE',  ( -1.000000000000000000, 0.000000000000000000, 0.000000000000000000 ) ) ;
#7556=PRESENTATION_STYLE_ASSIGNMENT (( #10358 ) ) ;
#7567=CARTESIAN_POINT ( 'NONE',  ( 4.078421086530217288, -3.990950201428958621, -1.000000000000000000 ) ) ;
#7574=ORIENTED_EDGE ( 'NONE', *, *, #6016, .T. ) ;
#7590=ORIENTED_EDGE ( 'NONE', *, *, #1906, .T. ) ;
#7653=CIRCLE ( 'NONE', #3441, 6.080745460913608902 ) ;
#7714=CARTESIAN_POINT ( 'NONE',  ( 0.000000000000000000, 0.000000000000000000, -1.000000000000000000 ) ) ;
#7721=VERTEX_POINT ( 'NONE', #9523 ) ;
#7738=ORIENTED_EDGE ( 'NONE', *, *, #9556, .F. ) ;
#7740=DIRECTION ( 'NONE',  ( 0.000000000000000000, 0.000000000000000000, 1.000000000000000000 ) ) ;
#7756=VERTEX_POINT ( 'NONE', #5708 ) ;
#7801=CYLINDRICAL_SURFACE ( 'NONE', #1021, 6.080745460913608902 ) ;
#7804=AXIS2_PLACEMENT_3D ( 'NONE', #6034, #2143, #11828 ) ;
#7809=ORIENTED_EDGE ( 'NONE', *, *, #5661, .T. ) ;
#7822=FACE_OUTER_BOUND ( 'NONE', #6523, .T. ) ;
#7826=VECTOR ( 'NONE', #7532, 1000.000000000000000 ) ;
#7834=VECTOR ( 'NONE', #10019, 1000.000000000000000 ) ;
#7846=STYLED_ITEM ( 'NONE', ( #7556 ), #4814 ) ;
#7848=EDGE_LOOP ( 'NONE', ( #9027, #7100, #5327, #423 ) ) ;
#7854=AXIS2_PLACEMENT_3D ( 'NONE', #2949, #12310, #8581 ) ;
#7859=DIRECTION ( 'NONE',  ( 0.000000000000000000, 0.000000000000000000, 1.000000000000000000 ) ) ;
#7863=ORIENTED_EDGE ( 'NONE', *, *, #7988, .T. ) ;
#7891=CARTESIAN_POINT ( 'NONE',  ( 0.000000000000000000, 0.000000000000000000, -1.000000000000000000 ) ) ;
#7916=ORIENTED_EDGE ( 'NONE', *, *, #1634, .F. ) ;
#7941=CARTESIAN_POINT ( 'NONE',  ( -1.250000000000000000, -6.429618962271402616, -1.000000000000000000 ) ) ;
#7977=PLANE ( 'NONE',  #9973 ) ;
#7988=EDGE_CURVE ( 'NONE', #7142, #6930, #3115, .T. ) ;
#7995=AXIS2_PLACEMENT_3D ( 'NONE', #6530, #9409, #583 ) ;
#8013=EDGE_CURVE ( 'NONE', #10347, #8570, #10374, .T. ) ;
#8032=PRODUCT_DEFINITION_CONTEXT ( 'detailed design', #3702, 'design' ) ;
#8038=CIRCLE ( 'NONE', #2040, 8.099999999999999645 ) ;
#8065=ORIENTED_EDGE ( 'NONE', *, *, #2740, .T. ) ;
#8073=AXIS2_PLACEMENT_3D ( 'NONE', #7891, #1179, #11799 ) ;
#8089=EDGE_CURVE ( 'NONE', #2301, #10119, #5991, .T. ) ;
#8096=CARTESIAN_POINT ( 'NONE',  ( 4.799999999999999822, 0.000000000000000000, -1.000000000000000000 ) ) ;
#8113=ADVANCED_FACE ( 'NONE', ( #3405 ), #399, .T. ) ;
#8119=ORIENTED_EDGE ( 'NONE', *, *, #8240, .T. ) ;
#8129=DIRECTION ( 'NONE',  ( 0.000000000000000000, 0.000000000000000000, 1.000000000000000000 ) ) ;
#8141=ORIENTED_EDGE ( 'NONE', *, *, #11197, .T. ) ;
#8159=ORIENTED_EDGE ( 'NONE', *, *, #7144, .T. ) ;
#8192=CARTESIAN_POINT ( 'NONE',  ( 0.5000000000000000000, -6.429618962271402616, 0.000000000000000000 ) ) ;
#8206=EDGE_LOOP ( 'NONE', ( #5331, #11618, #7574, #1144 ) ) ;
#8211=CARTESIAN_POINT ( 'NONE',  ( 0.000000000000000000, 0.000000000000000000, 0.000000000000000000 ) ) ;
#8231=AXIS2_PLACEMENT_3D ( 'NONE', #11310, #2626, #11126 ) ;
#8240=EDGE_CURVE ( 'NONE', #279, #10710, #3003, .T. ) ;
#8283=ORIENTED_EDGE ( 'NONE', *, *, #11584, .F. ) ;
#8291=ADVANCED_FACE ( 'NONE', ( #6593 ), #10275, .T. ) ;
#8296=CARTESIAN_POINT ( 'NONE',  ( 4.078421086530217288, -3.990950201428958621, -1.000000000000000000 ) ) ;
#8299=ORIENTED_EDGE ( 'NONE', *, *, #6959, .T. ) ;
#8310=FACE_OUTER_BOUND ( 'NONE', #2849, .T. ) ;
#8327=EDGE_CURVE ( 'NONE', #10119, #331, #11326, .T. ) ;
#8334=DIRECTION ( 'NONE',  ( -0.000000000000000000, -0.000000000000000000, -1.000000000000000000 ) ) ;
#8339=ORIENTED_EDGE ( 'NONE', *, *, #4179, .F. ) ;
#8355=LINE ( 'NONE', #11337, #3402 ) ;
#8366=AXIS2_PLACEMENT_3D ( 'NONE', #5062, #11795, #8890 ) ;
#8369=EDGE_CURVE ( 'NONE', #5296, #11243, #1662, .T. ) ;
#8371=ORIENTED_EDGE ( 'NONE', *, *, #1269, .F. ) ;
#8400=CARTESIAN_POINT ( 'NONE',  ( 0.000000000000000000, 0.000000000000000000, -1.000000000000000000 ) ) ;
#8407=UNCERTAINTY_MEASURE_WITH_UNIT (LENGTH_MEASURE( 1.000000000000000082E-05 ), #6000, 'distance_accuracy_value', 'NONE');
#8414=ADVANCED_FACE ( 'NONE', ( #4903 ), #2907, .F. ) ;
#8427=ORIENTED_EDGE ( 'NONE', *, *, #11650, .F. ) ;
#8430=VECTOR ( 'NONE', #5677, 1000.000000000000000 ) ;
#8468=CARTESIAN_POINT ( 'NONE',  ( -2.000000000000000000, -6.429618962271402616, -1.000000000000000000 ) ) ;
#8488=ORIENTED_EDGE ( 'NONE', *, *, #1102, .F. ) ;
#8503=( NAMED_UNIT ( * ) PLANE_ANGLE_UNIT ( ) SI_UNIT ( $, .RADIAN. ) );
#8506=CARTESIAN_POINT ( 'NONE',  ( 0.000000000000000000, 0.5192545390863916310, 0.000000000000000000 ) ) ;
#8524=ADVANCED_FACE ( 'NONE', ( #9038 ), #4323, .T. ) ;
#8529=UNCERTAINTY_MEASURE_WITH_UNIT (LENGTH_MEASURE( 1.000000000000000082E-05 ), #1548, 'distance_accuracy_value', 'NONE');
#8541=DIRECTION ( 'NONE',  ( 0.000000000000000000, 0.000000000000000000, 1.000000000000000000 ) ) ;
#8552=DIRECTION ( 'NONE',  ( 1.000000000000000000, 0.000000000000000000, 0.000000000000000000 ) ) ;
#8570=VERTEX_POINT ( 'NONE', #3576 ) ;
#8580=LINE ( 'NONE', #3705, #2307 ) ;
#8581=DIRECTION ( 'NONE',  ( 1.000000000000000000, 0.000000000000000000, 0.000000000000000000 ) ) ;
#8592=EDGE_CURVE ( 'NONE', #7124, #1873, #10000, .T. ) ;
#8596=DIRECTION ( 'NONE',  ( 1.000000000000000000, 0.000000000000000000, 0.000000000000000000 ) ) ;
#8626=AXIS2_PLACEMENT_3D ( 'NONE', #2953, #11452, #10707 ) ;
#8631=EDGE_CURVE ( 'NONE', #4672, #4056, #6333, .T. ) ;
#8666=CARTESIAN_POINT ( 'NONE',  ( 0.000000000000000000, 0.5192545390863916310, -1.000000000000000000 ) ) ;
#8667=CARTESIAN_POINT ( 'NONE',  ( -2.354826896168714434, -6.962563485461402024, 0.000000000000000000 ) ) ;
#8679=ORIENTED_EDGE ( 'NONE', *, *, #9369, .F. ) ;
#8681=CARTESIAN_POINT ( 'NONE',  ( 2.354826896168714434, -6.962563485461402024, -1.000000000000000000 ) ) ;
#8704=DIRECTION ( 'NONE',  ( 1.000000000000000000, 0.000000000000000000, -0.000000000000000000 ) ) ;
#8709=LINE ( 'NONE', #2079, #6207 ) ;
#8719=ORIENTED_EDGE ( 'NONE', *, *, #11568, .F. ) ;
#8720=DIRECTION ( 'NONE',  ( 0.000000000000000000, 0.000000000000000000, 1.000000000000000000 ) ) ;
#8724=PRODUCT_DEFINITION_SHAPE ( 'NONE', 'NONE',  #11668 ) ;
#8735=DIRECTION ( 'NONE',  ( 0.1305261922200524338, 0.9914448613738102711, 0.000000000000000000 ) ) ;
#8761=AXIS2_PLACEMENT_3D ( 'NONE', #8506, #1996, #4686 ) ;
#8780=CARTESIAN_POINT ( 'NONE',  ( 3.098410542199072637, -7.060458129626440815, -1.000000000000000000 ) ) ;
#8804=VECTOR ( 'NONE', #12252, 1000.000000000000000 ) ;
#8821=ORIENTED_EDGE ( 'NONE', *, *, #6519, .T. ) ;
#8857=CIRCLE ( 'NONE', #10643, 0.7500000000000000000 ) ;
#8864=DIRECTION ( 'NONE',  ( 1.000000000000000000, 0.000000000000000000, 0.000000000000000000 ) ) ;
#8890=DIRECTION ( 'NONE',  ( 1.000000000000000000, 0.000000000000000000, 0.000000000000000000 ) ) ;
#8943=ORIENTED_EDGE ( 'NONE', *, *, #2101, .T. ) ;
#8948=ORIENTED_EDGE ( 'NONE', *, *, #5115, .T. ) ;
#8964=CIRCLE ( 'NONE', #1556, 4.799999999999999822 ) ;
#8969=AXIS2_PLACEMENT_3D ( 'NONE', #9695, #5058, #2237 ) ;
#8992=AXIS2_PLACEMENT_3D ( 'NONE', #1907, #12319, #11392 ) ;
#8998=EDGE_CURVE ( 'NONE', #10979, #7124, #4364, .T. ) ;
#9027=ORIENTED_EDGE ( 'NONE', *, *, #10658, .F. ) ;
#9038=FACE_OUTER_BOUND ( 'NONE', #1150, .T. ) ;
#9093=CARTESIAN_POINT ( 'NONE',  ( 2.595115354961440524, -7.673029147243177306, -1.000000000000000000 ) ) ;
#9112=VERTEX_POINT ( 'NONE', #4918 ) ;
#9113=LINE ( 'NONE', #10274, #11556 ) ;
#9146=FACE_BOUND ( 'NONE', #2669, .T. ) ;
#9158=CARTESIAN_POINT ( 'NONE',  ( 0.2499999999999966416, -8.096141056083448362, -1.000000000000000000 ) ) ;
#9186=ORIENTED_EDGE ( 'NONE', *, *, #1063, .T. ) ;
#9202=CARTESIAN_POINT ( 'NONE',  ( -4.799999999999999822, 5.878304635907294211E-16, 0.000000000000000000 ) ) ;
#9229=CIRCLE ( 'NONE', #11014, 0.7499999999999997780 ) ;
#9248=CIRCLE ( 'NONE', #7249, 4.799999999999999822 ) ;
#9257=ORIENTED_EDGE ( 'NONE', *, *, #6223, .F. ) ;
#9262=EDGE_LOOP ( 'NONE', ( #10616, #5160, #9700, #3903 ) ) ;
#9267=DIRECTION ( 'NONE',  ( 1.000000000000000000, 0.000000000000000000, 0.000000000000000000 ) ) ;
#9275=ORIENTED_EDGE ( 'NONE', *, *, #8369, .T. ) ;
#9276=DIRECTION ( 'NONE',  ( -0.000000000000000000, -0.000000000000000000, -1.000000000000000000 ) ) ;
#9281=FACE_OUTER_BOUND ( 'NONE', #7848, .T. ) ;
#9288=CARTESIAN_POINT ( 'NONE',  ( 0.000000000000000000, 0.000000000000000000, 0.000000000000000000 ) ) ;
#9343=VERTEX_POINT ( 'NONE', #11845 ) ;
#9353=DIRECTION ( 'NONE',  ( 0.000000000000000000, 0.000000000000000000, 1.000000000000000000 ) ) ;
#9369=EDGE_CURVE ( 'NONE', #7721, #6749, #11616, .T. ) ;
#9409=DIRECTION ( 'NONE',  ( 0.000000000000000000, 0.000000000000000000, 1.000000000000000000 ) ) ;
#9425=CIRCLE ( 'NONE', #11808, 6.080745460913608902 ) ;
#9473=DIRECTION ( 'NONE',  ( -0.000000000000000000, -0.000000000000000000, -1.000000000000000000 ) ) ;
#9496=CARTESIAN_POINT ( 'NONE',  ( 0.000000000000000000, 0.5192545390863916310, -1.000000000000000000 ) ) ;
#9523=CARTESIAN_POINT ( 'NONE',  ( -2.595115354961444076, -7.673029147243174641, 0.000000000000000000 ) ) ;
#9556=EDGE_CURVE ( 'NONE', #8570, #9112, #9425, .T. ) ;
#9558=DIRECTION ( 'NONE',  ( 0.000000000000000000, 0.000000000000000000, 1.000000000000000000 ) ) ;
#9594=CARTESIAN_POINT ( 'NONE',  ( 0.000000000000000000, 0.000000000000000000, 0.000000000000000000 ) ) ;
#9622=EDGE_CURVE ( 'NONE', #4193, #10979, #2911, .T. ) ;
#9670=DIRECTION ( 'NONE',  ( 0.000000000000000000, 0.000000000000000000, 1.000000000000000000 ) ) ;
#9695=CARTESIAN_POINT ( 'NONE',  ( 0.000000000000000000, 0.000000000000000000, -1.000000000000000000 ) ) ;
#9700=ORIENTED_EDGE ( 'NONE', *, *, #658, .T. ) ;
#9728=DIRECTION ( 'NONE',  ( 0.000000000000000000, 0.000000000000000000, 1.000000000000000000 ) ) ;
#9754=DIRECTION ( 'NONE',  ( 1.000000000000000000, 0.000000000000000000, 0.000000000000000000 ) ) ;
#9778=VECTOR ( 'NONE', #8129, 1000.000000000000000 ) ;
#9787=AXIS2_PLACEMENT_3D ( 'NONE', #5043, #337, #4102 ) ;
#9799=DIRECTION ( 'NONE',  ( 0.1305261922200524616, -0.9914448613738103822, 0.000000000000000000 ) ) ;
#9817=AXIS2_PLACEMENT_3D ( 'NONE', #3040, #4780, #5721 ) ;
#9837=CIRCLE ( 'NONE', #4431, 2.396904916527699214 ) ;
#9838=EDGE_CURVE ( 'NONE', #4672, #4082, #9248, .T. ) ;
#9848=CARTESIAN_POINT ( 'NONE',  ( 5.686050877451574337, -5.768780236673276995, -1.000000000000000000 ) ) ;
#9879=AXIS2_PLACEMENT_3D ( 'NONE', #2332, #6041, #5972 ) ;
#9919=EDGE_CURVE ( 'NONE', #279, #3487, #4649, .T. ) ;
#9945=CARTESIAN_POINT ( 'NONE',  ( -1.250000000000000000, -6.429618962271402616, 0.000000000000000000 ) ) ;
#9948=ORIENTED_EDGE ( 'NONE', *, *, #38, .T. ) ;
#9962=DIRECTION ( 'NONE',  ( 0.000000000000000000, 0.000000000000000000, 1.000000000000000000 ) ) ;
#9971=ADVANCED_FACE ( 'NONE', ( #11635 ), #4828, .F. ) ;
#9973=AXIS2_PLACEMENT_3D ( 'NONE', #1337, #2218, #10724 ) ;
#10000=CIRCLE ( 'NONE', #4596, 8.099999999999999645 ) ;
#10019=DIRECTION ( 'NONE',  ( 0.000000000000000000, 0.000000000000000000, 1.000000000000000000 ) ) ;
#10033=VECTOR ( 'NONE', #6731, 1000.000000000000114 ) ;
#10036=ORIENTED_EDGE ( 'NONE', *, *, #8327, .T. ) ;
#10063=MECHANICAL_DESIGN_GEOMETRIC_PRESENTATION_REPRESENTATION('',(#3083),#6072);
#10077=AXIS2_PLACEMENT_3D ( 'NONE', #9848, #1201, #11878 ) ;
#10119=VERTEX_POINT ( 'NONE', #7016 ) ;
#10133=VERTEX_POINT ( 'NONE', #5262 ) ;
#10145=ORIENTED_EDGE ( 'NONE', *, *, #9369, .T. ) ;
#10155=CIRCLE ( 'NONE', #8761, 6.080745460913608902 ) ;
#10173=AXIS2_PLACEMENT_3D ( 'NONE', #12237, #2738, #4687 ) ;
#10218=DIRECTION ( 'NONE',  ( 0.000000000000000000, 0.000000000000000000, 1.000000000000000000 ) ) ;
#10219=( GEOMETRIC_REPRESENTATION_CONTEXT ( 3 ) GLOBAL_UNCERTAINTY_ASSIGNED_CONTEXT ( ( #3767 ) ) GLOBAL_UNIT_ASSIGNED_CONTEXT ( ( #4615, #8503, #4547 ) ) REPRESENTATION_CONTEXT ( 'NONE', 'WORKASPACE' ) );
#10225=ORIENTED_EDGE ( 'NONE', *, *, #7988, .F. ) ;
#10251=EDGE_LOOP ( 'NONE', ( #211, #3769, #2054, #4812 ) ) ;
#10264=DIRECTION ( 'NONE',  ( 1.000000000000000000, 0.000000000000000000, 0.000000000000000000 ) ) ;
#10274=CARTESIAN_POINT ( 'NONE',  ( -0.2500000000000000000, -8.096141056083446585, -1.000000000000000000 ) ) ;
#10275=CYLINDRICAL_SURFACE ( 'NONE', #7995, 6.080745460913608902 ) ;
#10347=VERTEX_POINT ( 'NONE', #7567 ) ;
#10358=SURFACE_STYLE_USAGE ( .BOTH. , #3874 ) ;
#10374=CIRCLE ( 'NONE', #10972, 6.080745460913608902 ) ;
#10383=DIRECTION ( 'NONE',  ( 1.000000000000000000, 0.000000000000000000, 0.000000000000000000 ) ) ;
#10403=EDGE_LOOP ( 'NONE', ( #3327, #176, #10672, #967 ) ) ;
#10415=VECTOR ( 'NONE', #9962, 1000.000000000000000 ) ;
#10437=CARTESIAN_POINT ( 'NONE',  ( 4.799999999999999822, 0.000000000000000000, -1.000000000000000000 ) ) ;
#10443=DIRECTION ( 'NONE',  ( 1.000000000000000000, 0.000000000000000000, 0.000000000000000000 ) ) ;
#10476=ORIENTED_EDGE ( 'NONE', *, *, #11568, .T. ) ;
#10520=ORIENTED_EDGE ( 'NONE', *, *, #11650, .T. ) ;
#10546=ORIENTED_EDGE ( 'NONE', *, *, #485, .F. ) ;
#10567=CLOSED_SHELL ( 'NONE', ( #431, #9971, #8291, #1908, #4304, #11324, #12322, #6163, #412, #10748, #35, #1895, #1140, #10722, #1077, #8524, #1991, #8113, #4611, #5231, #8414, #3880 ) ) ;
#10569=DIRECTION ( 'NONE',  ( 0.000000000000000000, 0.000000000000000000, 1.000000000000000000 ) ) ;
#10583=AXIS2_PLACEMENT_3D ( 'NONE', #4217, #11955, #470 ) ;
#10606=PLANE ( 'NONE',  #1009 ) ;
#10616=ORIENTED_EDGE ( 'NONE', *, *, #8631, .F. ) ;
#10643=AXIS2_PLACEMENT_3D ( 'NONE', #1667, #8541, #3781 ) ;
#10653=FACE_OUTER_BOUND ( 'NONE', #9262, .T. ) ;
#10658=EDGE_CURVE ( 'NONE', #477, #4908, #11151, .T. ) ;
#10672=ORIENTED_EDGE ( 'NONE', *, *, #2946, .T. ) ;
#10700=EDGE_CURVE ( 'NONE', #7142, #4908, #5432, .T. ) ;
#10707=DIRECTION ( 'NONE',  ( 1.000000000000000000, 0.000000000000000000, 0.000000000000000000 ) ) ;
#10710=VERTEX_POINT ( 'NONE', #3362 ) ;
#10722=ADVANCED_FACE ( 'NONE', ( #2424 ), #5309, .F. ) ;
#10724=DIRECTION ( 'NONE',  ( 0.1305261922200524338, -0.9914448613738102711, 0.000000000000000000 ) ) ;
#10746=VECTOR ( 'NONE', #276, 1000.000000000000000 ) ;
#10748=ADVANCED_FACE ( 'NONE', ( #8310 ), #4544, .T. ) ;
#10783=DIRECTION ( 'NONE',  ( 0.000000000000000000, 0.000000000000000000, 1.000000000000000000 ) ) ;
#10793=LINE ( 'NONE', #4114, #4825 ) ;
#10823=DIRECTION ( 'NONE',  ( 0.1305261922200524616, -0.9914448613738103822, 0.000000000000000000 ) ) ;
#10852=AXIS2_PLACEMENT_3D ( 'NONE', #12302, #6646, #10443 ) ;
#10870=ORIENTED_EDGE ( 'NONE', *, *, #7144, .F. ) ;
#10897=LINE ( 'NONE', #6147, #10415 ) ;
#10940=DIRECTION ( 'NONE',  ( 1.000000000000000000, 0.000000000000000000, 0.000000000000000000 ) ) ;
#10972=AXIS2_PLACEMENT_3D ( 'NONE', #1983, #1045, #11593 ) ;
#10979=VERTEX_POINT ( 'NONE', #9158 ) ;
#11014=AXIS2_PLACEMENT_3D ( 'NONE', #8667, #9670, #150 ) ;
#11070=ORIENTED_EDGE ( 'NONE', *, *, #2739, .F. ) ;
#11089=CARTESIAN_POINT ( 'NONE',  ( -4.799999999999999822, 5.878304635907294211E-16, -1.000000000000000000 ) ) ;
#11102=LINE ( 'NONE', #5301, #2825 ) ;
#11108=CARTESIAN_POINT ( 'NONE',  ( -2.354826896168714434, -6.962563485461402024, -1.000000000000000000 ) ) ;
#11114=ORIENTED_EDGE ( 'NONE', *, *, #6016, .F. ) ;
#11126=DIRECTION ( 'NONE',  ( 1.000000000000000000, 0.000000000000000000, 0.000000000000000000 ) ) ;
#11129=FACE_BOUND ( 'NONE', #467, .T. ) ;
#11151=CIRCLE ( 'NONE', #8366, 2.396904916527700102 ) ;
#11160=PLANE ( 'NONE',  #2028 ) ;
#11164=DIRECTION ( 'NONE',  ( 1.000000000000000000, 0.000000000000000000, 0.000000000000000000 ) ) ;
#11185=AXIS2_PLACEMENT_3D ( 'NONE', #1543, #12043, #11164 ) ;
#11197=EDGE_CURVE ( 'NONE', #4830, #6538, #2617, .T. ) ;
#11208=CIRCLE ( 'NONE', #8231, 6.080745460913608902 ) ;
#11216=LINE ( 'NONE', #91, #7826 ) ;
#11221=LINE ( 'NONE', #2663, #1221 ) ;
#11243=VERTEX_POINT ( 'NONE', #11385 ) ;
#11254=CARTESIAN_POINT ( 'NONE',  ( 3.309651814758565180, -5.455921364805393026, -1.000000000000000000 ) ) ;
#11280=EDGE_LOOP ( 'NONE', ( #5207, #11959, #8159, #10476 ) ) ;
#11299=SURFACE_STYLE_FILL_AREA ( #12292 ) ;
#11310=CARTESIAN_POINT ( 'NONE',  ( 0.000000000000000000, 0.5192545390863916310, 0.000000000000000000 ) ) ;
#11315=DIRECTION ( 'NONE',  ( 1.000000000000000000, 0.000000000000000000, 0.000000000000000000 ) ) ;
#11324=ADVANCED_FACE ( 'NONE', ( #10653 ), #2832, .F. ) ;
#11326=LINE ( 'NONE', #3594, #2591 ) ;
#11337=CARTESIAN_POINT ( 'NONE',  ( -0.1481481481481481122, -4.797713218419819903, -1.000000000000000000 ) ) ;
#11372=ORIENTED_EDGE ( 'NONE', *, *, #4957, .T. ) ;
#11385=CARTESIAN_POINT ( 'NONE',  ( 3.309651814758564736, -5.455921364805393026, 0.000000000000000000 ) ) ;
#11391=VECTOR ( 'NONE', #4046, 1000.000000000000000 ) ;
#11392=DIRECTION ( 'NONE',  ( 1.000000000000000000, 0.000000000000000000, 0.000000000000000000 ) ) ;
#11452=DIRECTION ( 'NONE',  ( 0.000000000000000000, 0.000000000000000000, 1.000000000000000000 ) ) ;
#11500=DIRECTION ( 'NONE',  ( 0.000000000000000000, 0.000000000000000000, 1.000000000000000000 ) ) ;
#11547=EDGE_LOOP ( 'NONE', ( #6275, #204, #7809, #907 ) ) ;
#11556=VECTOR ( 'NONE', #10218, 1000.000000000000000 ) ;
#11560=AXIS2_PLACEMENT_3D ( 'NONE', #4280, #3232, #6292 ) ;
#11568=EDGE_CURVE ( 'NONE', #3494, #1873, #6200, .T. ) ;
#11584=EDGE_CURVE ( 'NONE', #6497, #5098, #11208, .T. ) ;
#11593=DIRECTION ( 'NONE',  ( 1.000000000000000000, 0.000000000000000000, 0.000000000000000000 ) ) ;
#11599=CARTESIAN_POINT ( 'NONE',  ( 2.000000000000000000, -6.429618962271402616, -1.000000000000000000 ) ) ;
#11616=CIRCLE ( 'NONE', #5433, 8.099999999999999645 ) ;
#11618=ORIENTED_EDGE ( 'NONE', *, *, #127, .F. ) ;
#11635=FACE_OUTER_BOUND ( 'NONE', #6526, .T. ) ;
#11650=EDGE_CURVE ( 'NONE', #9343, #7721, #744, .T. ) ;
#11653=EDGE_LOOP ( 'NONE', ( #8339, #11114, #9257, #11707, #10225, #6307, #5597, #7738, #5895, #5173, #1095, #1973, #10870, #12130, #4410, #12316 ) ) ;
#11667=ORIENTED_EDGE ( 'NONE', *, *, #6519, .F. ) ;
#11668=PRODUCT_DEFINITION ( 'UNKNOWN', '', #11819, #8032 ) ;
#11674=CARTESIAN_POINT ( 'NONE',  ( -3.309651814758565180, -5.455921364805393026, -1.000000000000000000 ) ) ;
#11677=EDGE_CURVE ( 'NONE', #6198, #6377, #2557, .T. ) ;
#11707=ORIENTED_EDGE ( 'NONE', *, *, #283, .F. ) ;
#11709=EDGE_CURVE ( 'NONE', #1937, #7142, #1237, .T. ) ;
#11752=APPLICATION_CONTEXT ( 'automotive_design' ) ;
#11769=ORIENTED_EDGE ( 'NONE', *, *, #8089, .T. ) ;
#11782=ORIENTED_EDGE ( 'NONE', *, *, #5003, .T. ) ;
#11790=AXIS2_PLACEMENT_3D ( 'NONE', #4606, #5603, #601 ) ;
#11795=DIRECTION ( 'NONE',  ( -0.000000000000000000, -0.000000000000000000, -1.000000000000000000 ) ) ;
#11799=DIRECTION ( 'NONE',  ( 1.000000000000000000, 0.000000000000000000, 0.000000000000000000 ) ) ;
#11808=AXIS2_PLACEMENT_3D ( 'NONE', #8666, #7859, #8596 ) ;
#11819=PRODUCT_DEFINITION_FORMATION_WITH_SPECIFIED_SOURCE ( 'ANY', '', #132, .NOT_KNOWN. ) ;
#11825=ORIENTED_EDGE ( 'NONE', *, *, #9622, .T. ) ;
#11828=DIRECTION ( 'NONE',  ( 1.000000000000000000, 0.000000000000000000, 0.000000000000000000 ) ) ;
#11838=VERTEX_POINT ( 'NONE', #5696 ) ;
#11845=CARTESIAN_POINT ( 'NONE',  ( -2.595115354961444076, -7.673029147243174641, -1.000000000000000000 ) ) ;
#11878=DIRECTION ( 'NONE',  ( 1.000000000000000000, 0.000000000000000000, 0.000000000000000000 ) ) ;
#11897=CARTESIAN_POINT ( 'NONE',  ( 3.309651814758564736, -5.455921364805393026, -1.000000000000000000 ) ) ;
#11903=EDGE_LOOP ( 'NONE', ( #5434, #8948, #8141, #9186, #1103, #5738, #9275, #8821, #5312, #11969, #8299, #12312, #4778, #8065, #10145, #545 ) ) ;
#11905=EDGE_CURVE ( 'NONE', #9112, #1937, #7653, .T. ) ;
#11955=DIRECTION ( 'NONE',  ( -0.9995235871707960351, -0.03086419753086420970, 0.000000000000000000 ) ) ;
#11959=ORIENTED_EDGE ( 'NONE', *, *, #8998, .F. ) ;
#11969=ORIENTED_EDGE ( 'NONE', *, *, #11584, .T. ) ;
#11976=CARTESIAN_POINT ( 'NONE',  ( -3.309651814758565180, -5.455921364805393026, -1.000000000000000000 ) ) ;
#11988=CARTESIAN_POINT ( 'NONE',  ( 0.2499999999999966416, -8.096141056083448362, -1.000000000000000000 ) ) ;
#12043=DIRECTION ( 'NONE',  ( 0.000000000000000000, 0.000000000000000000, 1.000000000000000000 ) ) ;
#12047=CARTESIAN_POINT ( 'NONE',  ( 5.686050877451574337, -5.768780236673276995, -1.000000000000000000 ) ) ;
#12059=CARTESIAN_POINT ( 'NONE',  ( -0.1481481481481481122, -4.797713218419819903, 0.000000000000000000 ) ) ;
#12130=ORIENTED_EDGE ( 'NONE', *, *, #9622, .F. ) ;
#12151=CIRCLE ( 'NONE', #9787, 0.7500000000000000000 ) ;
#12154=EDGE_CURVE ( 'NONE', #1937, #477, #11221, .T. ) ;
#12166=VECTOR ( 'NONE', #3991, 1000.000000000000000 ) ;
#12173=AXIS2_PLACEMENT_3D ( 'NONE', #6912, #8720, #1146 ) ;
#12203=EDGE_CURVE ( 'NONE', #7536, #3487, #8857, .T. ) ;
#12212=ORIENTED_EDGE ( 'NONE', *, *, #8327, .F. ) ;
#12237=CARTESIAN_POINT ( 'NONE',  ( -1.250000000000000000, -6.429618962271402616, -1.000000000000000000 ) ) ;
#12252=DIRECTION ( 'NONE',  ( 0.000000000000000000, 0.000000000000000000, 1.000000000000000000 ) ) ;
#12253=FACE_OUTER_BOUND ( 'NONE', #11280, .T. ) ;
#12292=FILL_AREA_STYLE ('',( #864 ) ) ;
#12302=CARTESIAN_POINT ( 'NONE',  ( 0.000000000000000000, 0.5192545390863916310, 0.000000000000000000 ) ) ;
#12310=DIRECTION ( 'NONE',  ( 0.000000000000000000, 0.000000000000000000, 1.000000000000000000 ) ) ;
#12312=ORIENTED_EDGE ( 'NONE', *, *, #10658, .T. ) ;
#12316=ORIENTED_EDGE ( 'NONE', *, *, #9838, .F. ) ;
#12319=DIRECTION ( 'NONE',  ( 0.000000000000000000, 0.000000000000000000, 1.000000000000000000 ) ) ;
#12322=ADVANCED_FACE ( 'NONE', ( #2965 ), #29, .F. ) ;
#12392=COLOUR_RGB('Grey',0.48,0.52,0.57);
#12393=FILL_AREA_STYLE_COLOUR('',#12392);
#12394=FILL_AREA_STYLE('',(#12393));
#12395=SURFACE_STYLE_FILL_AREA(#12394);
#12396=SURFACE_SIDE_STYLE('',(#12395));
#12397=SURFACE_STYLE_USAGE(.BOTH.,#12396);
#12398=PRESENTATION_STYLE_ASSIGNMENT((#12397));
ENDSEC;
END-ISO-10303-21;
